ISO-10303-21;
HEADER;
FILE_DESCRIPTION (('STEP AP214'),
    '1' );
FILE_NAME ('Pivot body rivet.step',
    '2026-10-12T23:53:07',
    ( '' ),
    ( '' ),
    'SwSTEP 2.0',
    'SolidWorks 2024',
    '' );
FILE_SCHEMA (( 'AUTOMOTIVE_DESIGN' ));
ENDSEC;

DATA;
#173=TOROIDAL_SURFACE ( 'NONE', #9991, 0.06434668806854092205, 0.005000000000000000104 ) ;
#288=VECTOR ( 'NONE', #22622, 39.37007874015748143 ) ;
#427=ORIENTED_EDGE ( 'NONE', *, *, #16448, .F. ) ;
#522=EDGE_LOOP ( 'NONE', ( #22192, #34276, #11323, #16636 ) ) ;
#666=ADVANCED_FACE ( 'NONE', ( #19028 ), #1210, .T. ) ;
#819=AXIS2_PLACEMENT_3D ( 'NONE', #17406, #29967, #8743 ) ;
#945=ORIENTED_EDGE ( 'NONE', *, *, #20570, .T. ) ;
#1068=ORIENTED_EDGE ( 'NONE', *, *, #17280, .F. ) ;
#1103=VERTEX_POINT ( 'NONE', #2193 ) ;
#1126=( CONVERSION_BASED_UNIT ( 'INCH', #10967 ) LENGTH_UNIT ( ) NAMED_UNIT ( #23398 ) );
#1166=ADVANCED_FACE ( 'NONE', ( #18848, #18012 ), #37750, .T. ) ;
#1177=PRODUCT_DEFINITION ( 'UNKNOWN', '', #19398, #5857 ) ;
#1210=TOROIDAL_SURFACE ( 'NONE', #30078, 0.04249999999999999611, 0.02499999999999995628 ) ;
#1217=DIRECTION ( 'NONE',  ( 5.551115123125799958E-17, -4.553079989440443628E-16, -1.000000000000000000 ) ) ;
#1287=ORIENTED_EDGE ( 'NONE', *, *, #9712, .T. ) ;
#1462=FACE_OUTER_BOUND ( 'NONE', #19936, .T. ) ;
#1484=AXIS2_PLACEMENT_3D ( 'NONE', #17317, #35426, #26381 ) ;
#1506=CARTESIAN_POINT ( 'NONE',  ( 1.171686751963009499E-18, 0.2900000000000004796, 0.01749999999999952288 ) ) ;
#1543=EDGE_LOOP ( 'NONE', ( #19547, #20953, #31883, #36639 ) ) ;
#1612=EDGE_CURVE ( 'NONE', #8537, #36494, #9278, .T. ) ;
#1749=VERTEX_POINT ( 'NONE', #29551 ) ;
#1985=EDGE_LOOP ( 'NONE', ( #6775, #427, #21387, #33252 ) ) ;
#1992=ADVANCED_FACE ( 'NONE', ( #20718 ), #173, .T. ) ;
#2053=CARTESIAN_POINT ( 'NONE',  ( 2.048885995248197414E-16, 0.2900000000000004796, -5.122214988120493288E-16 ) ) ;
#2076=VECTOR ( 'NONE', #25527, 39.37007874015748854 ) ;
#2084=CIRCLE ( 'NONE', #12589, 0.06434668806854085266 ) ;
#2158=PRODUCT_DEFINITION_SHAPE ( 'NONE', 'NONE',  #1177 ) ;
#2180=AXIS2_PLACEMENT_3D ( 'NONE', #37451, #18535, #31091 ) ;
#2193=CARTESIAN_POINT ( 'NONE',  ( 5.487288226601811250E-16, -0.2899999999999993694, -0.04250000000000066225 ) ) ;
#2277=ORIENTED_EDGE ( 'NONE', *, *, #28847, .T. ) ;
#2294=AXIS2_PLACEMENT_3D ( 'NONE', #4735, #23299, #32728 ) ;
#2337=EDGE_LOOP ( 'NONE', ( #29855, #26571 ) ) ;
#2392=AXIS2_PLACEMENT_3D ( 'NONE', #35692, #23383, #16975 ) ;
#2421=TOROIDAL_SURFACE ( 'NONE', #38555, 0.04249999999999999611, 0.02499999999999995628 ) ;
#2513=CARTESIAN_POINT ( 'NONE',  ( 5.687846274369038479E-16, -0.3059742766594579222, -0.06173076923076999123 ) ) ;
#2572=EDGE_LOOP ( 'NONE', ( #37486, #6900 ) ) ;
#2620=DIRECTION ( 'NONE',  ( 1.188678714063518227E-15, -1.000000000000000000, -3.263080277421930985E-16 ) ) ;
#2630=VERTEX_POINT ( 'NONE', #13317 ) ;
#2772=VERTEX_POINT ( 'NONE', #36945 ) ;
#2835=VERTEX_POINT ( 'NONE', #30778 ) ;
#2961=DIRECTION ( 'NONE',  ( 0.000000000000000000, 0.000000000000000000, 1.000000000000000000 ) ) ;
#2996=CONICAL_SURFACE ( 'NONE', #17434, 0.07499999999999991396, 0.6931599075767558293 ) ;
#3000=CYLINDRICAL_SURFACE ( 'NONE', #16128, 0.01750000000000000513 ) ;
#3375=CARTESIAN_POINT ( 'NONE',  ( 2.048885995248197414E-16, 0.2900000000000004796, -5.122214988120493288E-16 ) ) ;
#3446=ORIENTED_EDGE ( 'NONE', *, *, #1612, .T. ) ;
#3456=DIRECTION ( 'NONE',  ( 5.551115123125956498E-17, 0.000000000000000000, -1.000000000000000000 ) ) ;
#3548=CIRCLE ( 'NONE', #17325, 0.06173076923076910999 ) ;
#3593=ORIENTED_EDGE ( 'NONE', *, *, #21100, .F. ) ;
#3696=DIRECTION ( 'NONE',  ( 1.188678714063518227E-15, -1.000000000000000000, -3.263080277421930985E-16 ) ) ;
#3749=ORIENTED_EDGE ( 'NONE', *, *, #28234, .F. ) ;
#3843=ADVANCED_FACE ( 'NONE', ( #36651 ), #28609, .T. ) ;
#3962=ADVANCED_FACE ( 'NONE', ( #29564 ), #2996, .T. ) ;
#4009=ORIENTED_EDGE ( 'NONE', *, *, #5671, .T. ) ;
#4047=CARTESIAN_POINT ( 'NONE',  ( 1.989330125873876791E-16, 0.2981948553318908290, -0.06819284191469622558 ) ) ;
#4077=CARTESIAN_POINT ( 'NONE',  ( 1.024442997624098658E-15, -0.3059742766594579222, -1.570812596356951301E-15 ) ) ;
#4161=DIMENSIONAL_EXPONENTS ( 1.000000000000000000, 0.000000000000000000, 0.000000000000000000, 0.000000000000000000, 0.000000000000000000, 0.000000000000000000, 0.000000000000000000 ) ;
#4174=VECTOR ( 'NONE', #29719, 39.37007874015748143 ) ;
#4272=CYLINDRICAL_SURFACE ( 'NONE', #16661, 0.01750000000000000513 ) ;
#4320=CARTESIAN_POINT ( 'NONE',  ( 0.000000000000000000, 0.000000000000000000, 0.000000000000000000 ) ) ;
#4690=ORIENTED_EDGE ( 'NONE', *, *, #7717, .T. ) ;
#4735=CARTESIAN_POINT ( 'NONE',  ( 7.512581982576723358E-16, 0.3059742766594581997, -3.756290991288361679E-16 ) ) ;
#4782=CIRCLE ( 'NONE', #9373, 0.06819284191469469902 ) ;
#4856=CARTESIAN_POINT ( 'NONE',  ( 2.048885995248197414E-16, 0.2900000000000004796, -5.122214988120493288E-16 ) ) ;
#4993=ORIENTED_EDGE ( 'NONE', *, *, #28289, .T. ) ;
#5111=CARTESIAN_POINT ( 'NONE',  ( 7.512581982576723358E-16, -0.2981948553318921613, -3.414809992080329023E-16 ) ) ;
#5279=CIRCLE ( 'NONE', #19120, 0.02499999999999993894 ) ;
#5442=DIRECTION ( 'NONE',  ( 5.551115123125759899E-17, -4.553079989440443628E-16, -1.000000000000000000 ) ) ;
#5485=VERTEX_POINT ( 'NONE', #33485 ) ;
#5534=CIRCLE ( 'NONE', #7494, 0.04249999999999994754 ) ;
#5671=EDGE_CURVE ( 'NONE', #36494, #2835, #35954, .T. ) ;
#5857=PRODUCT_DEFINITION_CONTEXT ( 'detailed design', #15854, 'design' ) ;
#6117=EDGE_CURVE ( 'NONE', #27170, #11941, #29365, .T. ) ;
#6183=AXIS2_PLACEMENT_3D ( 'NONE', #11677, #2620, #27327 ) ;
#6329=ORIENTED_EDGE ( 'NONE', *, *, #28767, .F. ) ;
#6368=ORIENTED_EDGE ( 'NONE', *, *, #17280, .T. ) ;
#6442=CARTESIAN_POINT ( 'NONE',  ( 2.185478394931410575E-15, -0.2949999999999994293, -9.902948977032954413E-16 ) ) ;
#6626=CARTESIAN_POINT ( 'NONE',  ( 2.077341244938675305E-16, 0.2900000000000004796, 0.04249999999999943406 ) ) ;
#6704=AXIS2_PLACEMENT_3D ( 'NONE', #13980, #7188, #7609 ) ;
#6764=DIRECTION ( 'NONE',  ( -1.188678714063518227E-15, 1.000000000000000000, 3.263080277421930985E-16 ) ) ;
#6775=ORIENTED_EDGE ( 'NONE', *, *, #26995, .F. ) ;
#6900=ORIENTED_EDGE ( 'NONE', *, *, #13180, .T. ) ;
#6940=DIRECTION ( 'NONE',  ( 1.188678714063518227E-15, -1.000000000000000000, -3.263080277421930985E-16 ) ) ;
#7186=PLANE ( 'NONE',  #38317 ) ;
#7188=DIRECTION ( 'NONE',  ( 1.188678714063518227E-15, -1.000000000000000000, -3.263080277421930985E-16 ) ) ;
#7199=ORIENTED_EDGE ( 'NONE', *, *, #40075, .F. ) ;
#7443=ADVANCED_FACE ( 'NONE', ( #25596 ), #16442, .T. ) ;
#7494=AXIS2_PLACEMENT_3D ( 'NONE', #33027, #17401, #10612 ) ;
#7569=TOROIDAL_SURFACE ( 'NONE', #37157, 0.04249999999999999611, 0.02499999999999995628 ) ;
#7583=ORIENTED_EDGE ( 'NONE', *, *, #28824, .F. ) ;
#7609=DIRECTION ( 'NONE',  ( 5.551115123125703816E-17, -5.306893166658304503E-16, -1.000000000000000000 ) ) ;
#7717=EDGE_CURVE ( 'NONE', #7737, #40210, #17293, .T. ) ;
#7737=VERTEX_POINT ( 'NONE', #29636 ) ;
#7825=DIRECTION ( 'NONE',  ( 1.188678714063518227E-15, -1.000000000000000000, -3.263080277421930985E-16 ) ) ;
#7952=DIRECTION ( 'NONE',  ( 1.188678714063518227E-15, -1.000000000000000000, -3.263080277421930985E-16 ) ) ;
#7996=AXIS2_PLACEMENT_3D ( 'NONE', #38051, #34356, #12153 ) ;
#8136=EDGE_LOOP ( 'NONE', ( #31236, #33995, #2277, #13999 ) ) ;
#8150=CIRCLE ( 'NONE', #26554, 0.06434668806854085266 ) ;
#8157=DIRECTION ( 'NONE',  ( 1.188678714063518227E-15, -1.000000000000000000, -3.263080277421930985E-16 ) ) ;
#8315=DIRECTION ( 'NONE',  ( 1.000000000000000000, 0.000000000000000000, 0.000000000000000000 ) ) ;
#8537=VERTEX_POINT ( 'NONE', #31421 ) ;
#8598=CARTESIAN_POINT ( 'NONE',  ( 4.823816367165299356E-16, 0.2949999999999992073, 0.06434668806854010326 ) ) ;
#8722=AXIS2_PLACEMENT_3D ( 'NONE', #14998, #9215, #27747 ) ;
#8732=CIRCLE ( 'NONE', #31741, 0.01750000000000001554 ) ;
#8743=DIRECTION ( 'NONE',  ( -5.551115123125856658E-17, 5.007578356027541926E-16, 1.000000000000000000 ) ) ;
#8746=DIRECTION ( 'NONE',  ( 5.551115123125788865E-17, -3.676620095425087714E-16, -1.000000000000000000 ) ) ;
#8898=ORIENTED_EDGE ( 'NONE', *, *, #38358, .F. ) ;
#8920=CARTESIAN_POINT ( 'NONE',  ( 0.000000000000000000, 0.000000000000000000, 0.000000000000000000 ) ) ;
#8925=AXIS2_PLACEMENT_3D ( 'NONE', #19702, #22404, #16232 ) ;
#8962=CARTESIAN_POINT ( 'NONE',  ( 4.780733988912460139E-16, 0.2949999999999991518, -7.512581982576723358E-16 ) ) ;
#8990=ADVANCED_FACE ( 'NONE', ( #11438 ), #38194, .T. ) ;
#9054=DIRECTION ( 'NONE',  ( 1.188678714063518227E-15, -1.000000000000000000, -3.263080277421930985E-16 ) ) ;
#9196=DIRECTION ( 'NONE',  ( -8.788982220891970033E-16, 0.7692307692307691624, -0.6389710663783134681 ) ) ;
#9215=DIRECTION ( 'NONE',  ( 1.188678714063518227E-15, -1.000000000000000000, -3.263080277421930985E-16 ) ) ;
#9278=CIRCLE ( 'NONE', #21132, 0.01750000000000001554 ) ;
#9373=AXIS2_PLACEMENT_3D ( 'NONE', #9638, #31644, #33936 ) ;
#9569=FACE_OUTER_BOUND ( 'NONE', #522, .T. ) ;
#9638=CARTESIAN_POINT ( 'NONE',  ( 2.048885995248197414E-16, 0.2981948553318907735, -1.707404996040164512E-16 ) ) ;
#9712=EDGE_CURVE ( 'NONE', #2630, #17210, #39531, .T. ) ;
#9941=EDGE_CURVE ( 'NONE', #2835, #1749, #24436, .T. ) ;
#9980=AXIS2_PLACEMENT_3D ( 'NONE', #20610, #11940, #36824 ) ;
#9991=AXIS2_PLACEMENT_3D ( 'NONE', #8962, #37150, #21535 ) ;
#10059=FACE_OUTER_BOUND ( 'NONE', #21577, .T. ) ;
#10108=CARTESIAN_POINT ( 'NONE',  ( 5.439739711127286542E-16, -0.2981948553318921613, 0.06819284191469295042 ) ) ;
#10265=ADVANCED_FACE ( 'NONE', ( #14230 ), #26433, .T. ) ;
#10370=ORIENTED_EDGE ( 'NONE', *, *, #33878, .T. ) ;
#10395=DIRECTION ( 'NONE',  ( 1.188678714063518424E-15, -1.000000000000000000, 0.000000000000000000 ) ) ;
#10612=DIRECTION ( 'NONE',  ( 5.551115123125774690E-17, 0.000000000000000000, -1.000000000000000000 ) ) ;
#10740=VECTOR ( 'NONE', #16978, 39.37007874015748854 ) ;
#10811=LINE ( 'NONE', #30331, #10740 ) ;
#10823=DIRECTION ( 'NONE',  ( 1.188678714063518227E-15, -1.000000000000000000, -3.263080277421930985E-16 ) ) ;
#10848=DIRECTION ( 'NONE',  ( 5.551115123125673617E-17, 3.263080277421931478E-16, -1.000000000000000000 ) ) ;
#10967=LENGTH_MEASURE_WITH_UNIT ( LENGTH_MEASURE( 0.02539999999999999897 ), #38919 );
#11034=CARTESIAN_POINT ( 'NONE',  ( 2.189050353664013844E-15, -0.2949999999999994849, -0.06434668806854183798 ) ) ;
#11078=EDGE_LOOP ( 'NONE', ( #3593, #18357 ) ) ;
#11111=APPLICATION_CONTEXT ( 'configuration controlled 3d designs of mechanical parts and assemblies' ) ;
#11260=ADVANCED_FACE ( 'NONE', ( #39688 ), #35671, .T. ) ;
#11294=CIRCLE ( 'NONE', #26429, 0.005000000000000014849 ) ;
#11323=ORIENTED_EDGE ( 'NONE', *, *, #11717, .T. ) ;
#11328=CIRCLE ( 'NONE', #6704, 0.06434668806854085266 ) ;
#11399=( GEOMETRIC_REPRESENTATION_CONTEXT ( 3 ) GLOBAL_UNCERTAINTY_ASSIGNED_CONTEXT ( ( #15737 ) ) GLOBAL_UNIT_ASSIGNED_CONTEXT ( ( #1126, #26195, #23112 ) ) REPRESENTATION_CONTEXT ( 'NONE', 'WORKASPACE' ) );
#11438=FACE_OUTER_BOUND ( 'NONE', #27695, .T. ) ;
#11637=DIRECTION ( 'NONE',  ( -1.000000000000000000, -1.188678714063518030E-15, -5.551115123125745108E-17 ) ) ;
#11643=DIRECTION ( 'NONE',  ( -1.188678714063518227E-15, 1.000000000000000000, 3.263080277421930985E-16 ) ) ;
#11677=CARTESIAN_POINT ( 'NONE',  ( 5.463695987328526437E-16, -0.2899999999999993694, -7.171100983368691195E-16 ) ) ;
#11717=EDGE_CURVE ( 'NONE', #8537, #2630, #23015, .T. ) ;
#11754=CARTESIAN_POINT ( 'NONE',  ( 5.463695987328526437E-16, -0.2899999999999993694, -7.171100983368691195E-16 ) ) ;
#11881=DIRECTION ( 'NONE',  ( 1.188678714063518227E-15, -1.000000000000000000, -3.263080277421930985E-16 ) ) ;
#11940=DIRECTION ( 'NONE',  ( 1.000000000000000000, 1.188678714063518030E-15, 5.551115123125745108E-17 ) ) ;
#11941=VERTEX_POINT ( 'NONE', #27322 ) ;
#12045=CARTESIAN_POINT ( 'NONE',  ( 5.463695987328526437E-16, -0.2899999999999993694, -7.171100983368691195E-16 ) ) ;
#12142=LINE ( 'NONE', #25094, #32436 ) ;
#12153=DIRECTION ( 'NONE',  ( 1.188678714063520199E-15, -1.000000000000000000, 0.000000000000000000 ) ) ;
#12171=DIRECTION ( 'NONE',  ( 5.551115123125718607E-17, 3.263080277421931478E-16, -1.000000000000000000 ) ) ;
#12402=DIRECTION ( 'NONE',  ( 1.188678714063518227E-15, -1.000000000000000000, -3.263080277421930985E-16 ) ) ;
#12445=CARTESIAN_POINT ( 'NONE',  ( 0.07500000000000131561, -0.2899999999999966493, -1.126887297386508504E-15 ) ) ;
#12589=AXIS2_PLACEMENT_3D ( 'NONE', #24666, #11881, #14782 ) ;
#12670=ORIENTED_EDGE ( 'NONE', *, *, #18217, .T. ) ;
#12838=EDGE_CURVE ( 'NONE', #23955, #1103, #31159, .T. ) ;
#12986=CARTESIAN_POINT ( 'NONE',  ( 1.024442997624098658E-15, -0.3059742766594579222, -1.570812596356951301E-15 ) ) ;
#12991=SHAPE_REPRESENTATION_RELATIONSHIP ( 'NONE' , 'NONE' ,  #35919, #37306 ) ;
#13002=EDGE_LOOP ( 'NONE', ( #16299, #39353, #18073, #28225 ) ) ;
#13033=DIRECTION ( 'NONE',  ( 1.000000000000000000, 1.188678714063518030E-15, -6.695352868347822093E-17 ) ) ;
#13055=DIRECTION ( 'NONE',  ( 5.551115123125673617E-17, 3.263080277421931478E-16, -1.000000000000000000 ) ) ;
#13134=DIRECTION ( 'NONE',  ( -1.188678714063518227E-15, 1.000000000000000000, 3.263080277421930985E-16 ) ) ;
#13180=EDGE_CURVE ( 'NONE', #13785, #2772, #8150, .T. ) ;
#13278=DIRECTION ( 'NONE',  ( -1.000000000000000000, -1.188678714063518030E-15, -5.551115123125745108E-17 ) ) ;
#13317=CARTESIAN_POINT ( 'NONE',  ( 5.473410438793996596E-16, -0.2899999999999993694, -0.01750000000000073372 ) ) ;
#13533=CARTESIAN_POINT ( 'NONE',  ( 5.463695987328526437E-16, -0.2899999999999993694, -7.171100983368691195E-16 ) ) ;
#13653=ORIENTED_EDGE ( 'NONE', *, *, #9941, .F. ) ;
#13738=ORIENTED_EDGE ( 'NONE', *, *, #24733, .F. ) ;
#13785=VERTEX_POINT ( 'NONE', #20788 ) ;
#13975=DIRECTION ( 'NONE',  ( 1.188678714063518227E-15, -1.000000000000000000, -3.263080277421930985E-16 ) ) ;
#13980=CARTESIAN_POINT ( 'NONE',  ( 5.463695987328526437E-16, -0.2899999999999993694, -7.171100983368691195E-16 ) ) ;
#13999=ORIENTED_EDGE ( 'NONE', *, *, #12838, .F. ) ;
#14142=DIRECTION ( 'NONE',  ( 1.188678714063518227E-15, -1.000000000000000000, -3.263080277421930985E-16 ) ) ;
#14230=FACE_OUTER_BOUND ( 'NONE', #16540, .T. ) ;
#14438=ORIENTED_EDGE ( 'NONE', *, *, #21100, .T. ) ;
#14516=VECTOR ( 'NONE', #9196, 39.37007874015748854 ) ;
#14549=CIRCLE ( 'NONE', #2180, 0.005000000000000014849 ) ;
#14594=VERTEX_POINT ( 'NONE', #37934 ) ;
#14633=( NAMED_UNIT ( * ) SI_UNIT ( $, .STERADIAN. ) SOLID_ANGLE_UNIT ( ) );
#14715=CIRCLE ( 'NONE', #37707, 0.02499999999999993894 ) ;
#14730=DIRECTION ( 'NONE',  ( -1.188678714063518227E-15, 1.000000000000000000, 3.263080277421930985E-16 ) ) ;
#14778=VERTEX_POINT ( 'NONE', #17551 ) ;
#14782=DIRECTION ( 'NONE',  ( 5.551115123125797493E-17, -5.306893166658304503E-16, -1.000000000000000000 ) ) ;
#14998=CARTESIAN_POINT ( 'NONE',  ( 5.463695987328526437E-16, -0.2899999999999993694, -7.171100983368691195E-16 ) ) ;
#15097=DIRECTION ( 'NONE',  ( 5.551115123125774690E-17, 0.000000000000000000, -1.000000000000000000 ) ) ;
#15596=LINE ( 'NONE', #37195, #14516 ) ;
#15611=DIRECTION ( 'NONE',  ( 1.000000000000000000, 1.188678714063518030E-15, -6.695352868347822093E-17 ) ) ;
#15657=FACE_OUTER_BOUND ( 'NONE', #31973, .T. ) ;
#15737=UNCERTAINTY_MEASURE_WITH_UNIT (LENGTH_MEASURE( 1.000000000000000082E-05 ), #1126, 'distance_accuracy_value', 'NONE');
#15854=APPLICATION_CONTEXT ( 'configuration controlled 3d designs of mechanical parts and assemblies' ) ;
#15864=FACE_OUTER_BOUND ( 'NONE', #2572, .T. ) ;
#16128=AXIS2_PLACEMENT_3D ( 'NONE', #40214, #31385, #8746 ) ;
#16232=DIRECTION ( 'NONE',  ( 5.551115123125783935E-17, 0.000000000000000000, -1.000000000000000000 ) ) ;
#16299=ORIENTED_EDGE ( 'NONE', *, *, #26115, .F. ) ;
#16442=TOROIDAL_SURFACE ( 'NONE', #36873, 0.06434668806854092205, 0.005000000000000000104 ) ;
#16448=EDGE_CURVE ( 'NONE', #40210, #5485, #18558, .T. ) ;
#16540=EDGE_LOOP ( 'NONE', ( #29924, #33511, #26412, #6329 ) ) ;
#16636=ORIENTED_EDGE ( 'NONE', *, *, #40075, .T. ) ;
#16642=CIRCLE ( 'NONE', #26484, 0.06819284191469469902 ) ;
#16661=AXIS2_PLACEMENT_3D ( 'NONE', #20327, #7952, #29990 ) ;
#16737=EDGE_CURVE ( 'NONE', #2772, #13785, #2084, .T. ) ;
#16948=ADVANCED_FACE ( 'NONE', ( #33197 ), #23556, .T. ) ;
#16975=DIRECTION ( 'NONE',  ( 5.551115123125868984E-17, -5.531779426422974156E-16, -1.000000000000000000 ) ) ;
#16978=DIRECTION ( 'NONE',  ( 9.571496092079945511E-16, -0.7692307692307691624, 0.6389710663783134681 ) ) ;
#17018=CARTESIAN_POINT ( 'NONE',  ( 2.845524969048586056E-18, 0.2900000000000004796, 0.04249999999999948957 ) ) ;
#17123=DIRECTION ( 'NONE',  ( 1.188678714063518227E-15, -1.000000000000000000, -3.263080277421930985E-16 ) ) ;
#17210=VERTEX_POINT ( 'NONE', #2513 ) ;
#17279=DIRECTION ( 'NONE',  ( 1.188678714063518227E-15, -1.000000000000000000, -3.263080277421930985E-16 ) ) ;
#17280=EDGE_CURVE ( 'NONE', #23808, #27248, #14549, .T. ) ;
#17285=DIRECTION ( 'NONE',  ( 5.551115123125956498E-17, 0.000000000000000000, -1.000000000000000000 ) ) ;
#17293=LINE ( 'NONE', #36418, #35483 ) ;
#17317=CARTESIAN_POINT ( 'NONE',  ( 4.780733988912460139E-16, 0.2949999999999991518, -7.512581982576723358E-16 ) ) ;
#17325=AXIS2_PLACEMENT_3D ( 'NONE', #4077, #3696, #22849 ) ;
#17329=DIRECTION ( 'NONE',  ( 5.551115123125703816E-17, -5.306893166658304503E-16, -1.000000000000000000 ) ) ;
#17401=DIRECTION ( 'NONE',  ( 1.188678714063518227E-15, -1.000000000000000000, -3.263080277421930985E-16 ) ) ;
#17406=CARTESIAN_POINT ( 'NONE',  ( 7.512581982576723358E-16, -0.2981948553318921613, -3.414809992080329023E-16 ) ) ;
#17434=AXIS2_PLACEMENT_3D ( 'NONE', #4856, #8157, #1217 ) ;
#17551=CARTESIAN_POINT ( 'NONE',  ( 5.499415574654559131E-16, -0.2899999999999994249, -0.06434668806854157430 ) ) ;
#17622=AXIS2_PLACEMENT_3D ( 'NONE', #12445, #21934, #33639 ) ;
#17666=DIRECTION ( 'NONE',  ( -5.551115123125856658E-17, 5.007578356027541926E-16, 1.000000000000000000 ) ) ;
#17814=CARTESIAN_POINT ( 'NONE',  ( 2.172611109905790102E-15, -0.2899999999999994249, 0.06434668806854020040 ) ) ;
#18011=FACE_OUTER_BOUND ( 'NONE', #13002, .T. ) ;
#18012=FACE_BOUND ( 'NONE', #26675, .T. ) ;
#18073=ORIENTED_EDGE ( 'NONE', *, *, #25547, .T. ) ;
#18217=EDGE_CURVE ( 'NONE', #14778, #27248, #11328, .T. ) ;
#18323=ORIENTED_EDGE ( 'NONE', *, *, #20318, .T. ) ;
#18357=ORIENTED_EDGE ( 'NONE', *, *, #6117, .F. ) ;
#18372=ORIENTED_EDGE ( 'NONE', *, *, #27805, .T. ) ;
#18441=ORIENTED_EDGE ( 'NONE', *, *, #28300, .T. ) ;
#18470=ORIENTED_EDGE ( 'NONE', *, *, #11717, .F. ) ;
#18535=DIRECTION ( 'NONE',  ( -1.000000000000000000, -1.188678714063518030E-15, -1.779758311459931231E-16 ) ) ;
#18558=CIRCLE ( 'NONE', #21209, 0.06819284191469469902 ) ;
#18848=FACE_OUTER_BOUND ( 'NONE', #2337, .T. ) ;
#19015=DIRECTION ( 'NONE',  ( 5.551115123125400598E-17, 3.263080277421932464E-16, -1.000000000000000000 ) ) ;
#19028=FACE_OUTER_BOUND ( 'NONE', #22757, .T. ) ;
#19120=AXIS2_PLACEMENT_3D ( 'NONE', #27881, #11637, #21096 ) ;
#19299=EDGE_CURVE ( 'NONE', #2835, #2630, #8732, .T. ) ;
#19398=PRODUCT_DEFINITION_FORMATION_WITH_SPECIFIED_SOURCE ( 'ANY', '', #21216, .NOT_KNOWN. ) ;
#19547=ORIENTED_EDGE ( 'NONE', *, *, #33826, .F. ) ;
#19548=DIRECTION ( 'NONE',  ( -5.551115123125767911E-17, 5.007578356027541926E-16, 1.000000000000000000 ) ) ;
#19572=DIRECTION ( 'NONE',  ( 5.551115123125788865E-17, -3.676620095425087221E-16, -1.000000000000000000 ) ) ;
#19702=CARTESIAN_POINT ( 'NONE',  ( 2.048885995248197414E-16, 0.2900000000000004796, -5.122214988120493288E-16 ) ) ;
#19726=EDGE_LOOP ( 'NONE', ( #7583, #31333, #4690, #25365 ) ) ;
#19936=EDGE_LOOP ( 'NONE', ( #14438, #18323, #29598, #21192 ) ) ;
#19960=CYLINDRICAL_SURFACE ( 'NONE', #35832, 0.04249999999999995448 ) ;
#20190=CARTESIAN_POINT ( 'NONE',  ( 2.845524969051194536E-18, -0.2899999999999993694, 0.04249999999999928141 ) ) ;
#20318=EDGE_CURVE ( 'NONE', #27170, #23955, #12142, .T. ) ;
#20327=CARTESIAN_POINT ( 'NONE',  ( 0.000000000000000000, 0.000000000000000000, 0.000000000000000000 ) ) ;
#20328=CARTESIAN_POINT ( 'NONE',  ( 1.171686751960861702E-18, 6.434085166993908708E-18, 0.01750000000000000513 ) ) ;
#20417=CONICAL_SURFACE ( 'NONE', #23711, 0.07499999999999991396, 0.6931599075767558293 ) ;
#20548=EDGE_LOOP ( 'NONE', ( #13653, #7199, #1287, #18372 ) ) ;
#20570=EDGE_CURVE ( 'NONE', #1749, #17210, #3548, .T. ) ;
#20610=CARTESIAN_POINT ( 'NONE',  ( 5.487288226601811250E-16, -0.2899999999999993694, -0.04250000000000066225 ) ) ;
#20718=FACE_OUTER_BOUND ( 'NONE', #1985, .T. ) ;
#20788=CARTESIAN_POINT ( 'NONE',  ( 4.835832620238532854E-16, 0.2900000000000004241, 0.06434668806854040857 ) ) ;
#20924=ORIENTED_EDGE ( 'NONE', *, *, #9941, .T. ) ;
#20953=ORIENTED_EDGE ( 'NONE', *, *, #38358, .T. ) ;
#21096=DIRECTION ( 'NONE',  ( 1.188678714063518819E-15, -1.000000000000000000, 0.000000000000000000 ) ) ;
#21100=EDGE_CURVE ( 'NONE', #11941, #27170, #5534, .T. ) ;
#21132=AXIS2_PLACEMENT_3D ( 'NONE', #27845, #12402, #37586 ) ;
#21192=ORIENTED_EDGE ( 'NONE', *, *, #28847, .F. ) ;
#21209=AXIS2_PLACEMENT_3D ( 'NONE', #28794, #6764, #19548 ) ;
#21216=PRODUCT ( 'Pivot body rivet', 'Pivot body rivet', '', ( #27756 ) ) ;
#21387=ORIENTED_EDGE ( 'NONE', *, *, #28767, .T. ) ;
#21449=DIRECTION ( 'NONE',  ( 1.188678714063518227E-15, -1.000000000000000000, -3.263080277421930985E-16 ) ) ;
#21535=DIRECTION ( 'NONE',  ( 5.551115123125663140E-17, 3.263080277421932464E-16, -1.000000000000000000 ) ) ;
#21557=ORIENTED_EDGE ( 'NONE', *, *, #28824, .T. ) ;
#21571=VERTEX_POINT ( 'NONE', #24296 ) ;
#21577=EDGE_LOOP ( 'NONE', ( #1068, #36356, #23448, #12670 ) ) ;
#21692=DIRECTION ( 'NONE',  ( -1.188678714063518227E-15, 1.000000000000000000, 3.263080277421930985E-16 ) ) ;
#21934=DIRECTION ( 'NONE',  ( -1.188678714063518030E-15, 1.000000000000000000, -3.676620095425087714E-16 ) ) ;
#22069=ADVANCED_FACE ( 'NONE', ( #18011 ), #20417, .T. ) ;
#22188=ORIENTED_EDGE ( 'NONE', *, *, #28234, .T. ) ;
#22192=ORIENTED_EDGE ( 'NONE', *, *, #5671, .F. ) ;
#22226=DIRECTION ( 'NONE',  ( 5.551115123125400598E-17, 3.263080277421932464E-16, -1.000000000000000000 ) ) ;
#22404=DIRECTION ( 'NONE',  ( 1.188678714063518227E-15, -1.000000000000000000, -3.263080277421930985E-16 ) ) ;
#22622=DIRECTION ( 'NONE',  ( 1.188678714063518227E-15, -1.000000000000000000, -3.263080277421930985E-16 ) ) ;
#22757=EDGE_LOOP ( 'NONE', ( #3446, #36205, #30823, #13738 ) ) ;
#22849=DIRECTION ( 'NONE',  ( 5.551115123125868984E-17, -5.531779426422974156E-16, -1.000000000000000000 ) ) ;
#23015=LINE ( 'NONE', #25691, #288 ) ;
#23030=TOROIDAL_SURFACE ( 'NONE', #24343, 0.06434668806854092205, 0.005000000000000000104 ) ;
#23112=( NAMED_UNIT ( * ) SI_UNIT ( $, .STERADIAN. ) SOLID_ANGLE_UNIT ( ) );
#23196=CIRCLE ( 'NONE', #38289, 0.01750000000000001554 ) ;
#23270=CIRCLE ( 'NONE', #28503, 0.005000000000000014849 ) ;
#23299=DIRECTION ( 'NONE',  ( 1.188678714063518227E-15, -1.000000000000000000, -3.263080277421930985E-16 ) ) ;
#23371=AXIS2_PLACEMENT_3D ( 'NONE', #11754, #27596, #36836 ) ;
#23383=DIRECTION ( 'NONE',  ( 1.188678714063518227E-15, -1.000000000000000000, -3.263080277421930985E-16 ) ) ;
#23398=DIMENSIONAL_EXPONENTS ( 1.000000000000000000, 0.000000000000000000, 0.000000000000000000, 0.000000000000000000, 0.000000000000000000, 0.000000000000000000, 0.000000000000000000 ) ;
#23422=DIRECTION ( 'NONE',  ( 1.188678714063518227E-15, -1.000000000000000000, -3.263080277421930985E-16 ) ) ;
#23448=ORIENTED_EDGE ( 'NONE', *, *, #29904, .T. ) ;
#23556=CYLINDRICAL_SURFACE ( 'NONE', #38966, 0.04249999999999995448 ) ;
#23601=ORIENTED_EDGE ( 'NONE', *, *, #12838, .T. ) ;
#23711=AXIS2_PLACEMENT_3D ( 'NONE', #34248, #14730, #39826 ) ;
#23742=DIRECTION ( 'NONE',  ( 5.551115123125790098E-17, -3.676620095425088700E-16, -1.000000000000000000 ) ) ;
#23808=VERTEX_POINT ( 'NONE', #10108 ) ;
#23955=VERTEX_POINT ( 'NONE', #20190 ) ;
#24092=VECTOR ( 'NONE', #14142, 39.37007874015748143 ) ;
#24143=ADVANCED_FACE ( 'NONE', ( #10059 ), #23030, .T. ) ;
#24268=DIRECTION ( 'NONE',  ( -1.188678714063518227E-15, 1.000000000000000000, 3.263080277421930985E-16 ) ) ;
#24296=CARTESIAN_POINT ( 'NONE',  ( 1.900334097155061703E-16, 0.3059742766594581997, 0.06173076923076874917 ) ) ;
#24343=AXIS2_PLACEMENT_3D ( 'NONE', #38036, #13134, #22226 ) ;
#24436=CIRCLE ( 'NONE', #7996, 0.02499999999999993894 ) ;
#24666=CARTESIAN_POINT ( 'NONE',  ( 2.048885995248197414E-16, 0.2900000000000004796, -5.122214988120493288E-16 ) ) ;
#24733=EDGE_CURVE ( 'NONE', #8537, #7737, #5279, .T. ) ;
#24915=LINE ( 'NONE', #28399, #2076 ) ;
#25094=CARTESIAN_POINT ( 'NONE',  ( 2.845524969047803358E-18, 1.562563540555661551E-17, 0.04249999999999995448 ) ) ;
#25174=AXIS2_PLACEMENT_3D ( 'NONE', #36455, #17123, #17329 ) ;
#25262=( GEOMETRIC_REPRESENTATION_CONTEXT ( 3 ) GLOBAL_UNCERTAINTY_ASSIGNED_CONTEXT ( ( #35074 ) ) GLOBAL_UNIT_ASSIGNED_CONTEXT ( ( #39522, #33359, #14633 ) ) REPRESENTATION_CONTEXT ( 'NONE', 'WORKASPACE' ) );
#25365=ORIENTED_EDGE ( 'NONE', *, *, #16448, .T. ) ;
#25527=DIRECTION ( 'NONE',  ( -1.028089648204243318E-15, 0.7692307692307690514, 0.6389710663783134681 ) ) ;
#25538=DIRECTION ( 'NONE',  ( -1.188678714063518227E-15, 1.000000000000000000, 3.263080277421930985E-16 ) ) ;
#25547=EDGE_CURVE ( 'NONE', #17210, #14594, #15596, .T. ) ;
#25596=FACE_OUTER_BOUND ( 'NONE', #26165, .T. ) ;
#25691=CARTESIAN_POINT ( 'NONE',  ( 9.714451465470134135E-19, -6.434085166993905626E-18, -0.01750000000000000513 ) ) ;
#25869=EDGE_CURVE ( 'NONE', #23808, #14594, #36244, .T. ) ;
#25956=DIRECTION ( 'NONE',  ( 5.551115123125790098E-17, -3.676620095425088700E-16, -1.000000000000000000 ) ) ;
#26115=EDGE_CURVE ( 'NONE', #1749, #23808, #24915, .T. ) ;
#26165=EDGE_LOOP ( 'NONE', ( #22188, #6368, #10370, #38453 ) ) ;
#26195=( NAMED_UNIT ( * ) PLANE_ANGLE_UNIT ( ) SI_UNIT ( $, .RADIAN. ) );
#26381=DIRECTION ( 'NONE',  ( 5.551115123125663140E-17, 3.263080277421932464E-16, -1.000000000000000000 ) ) ;
#26412=ORIENTED_EDGE ( 'NONE', *, *, #16737, .F. ) ;
#26429=AXIS2_PLACEMENT_3D ( 'NONE', #8598, #15611, #33931 ) ;
#26433=TOROIDAL_SURFACE ( 'NONE', #1484, 0.06434668806854092205, 0.005000000000000000104 ) ;
#26443=CARTESIAN_POINT ( 'NONE',  ( 2.359223927328458203E-18, -1.562563540555660935E-17, -0.04249999999999995448 ) ) ;
#26484=AXIS2_PLACEMENT_3D ( 'NONE', #5111, #24268, #17666 ) ;
#26499=CIRCLE ( 'NONE', #25174, 0.06434668806854085266 ) ;
#26554=AXIS2_PLACEMENT_3D ( 'NONE', #38990, #10823, #26671 ) ;
#26571=ORIENTED_EDGE ( 'NONE', *, *, #33878, .F. ) ;
#26671=DIRECTION ( 'NONE',  ( 5.551115123125797493E-17, -5.306893166658304503E-16, -1.000000000000000000 ) ) ;
#26675=EDGE_LOOP ( 'NONE', ( #18441, #23601 ) ) ;
#26991=LENGTH_MEASURE_WITH_UNIT ( LENGTH_MEASURE( 0.02539999999999999897 ), #34167 );
#26995=EDGE_CURVE ( 'NONE', #5485, #13785, #11294, .T. ) ;
#27065=DIRECTION ( 'NONE',  ( -1.188678714063530652E-15, 1.000000000000000000, 0.000000000000000000 ) ) ;
#27170=VERTEX_POINT ( 'NONE', #17018 ) ;
#27195=AXIS2_PLACEMENT_3D ( 'NONE', #29114, #13278, #10395 ) ;
#27239=DIRECTION ( 'NONE',  ( 1.188678714063518227E-15, -1.000000000000000000, -3.263080277421930985E-16 ) ) ;
#27248=VERTEX_POINT ( 'NONE', #17814 ) ;
#27267=EDGE_LOOP ( 'NONE', ( #8898, #4009, #35569, #18470 ) ) ;
#27322=CARTESIAN_POINT ( 'NONE',  ( 2.072478234521481980E-16, 0.2900000000000004796, -0.04250000000000046102 ) ) ;
#27327=DIRECTION ( 'NONE',  ( 5.551115123125845564E-17, 0.000000000000000000, -1.000000000000000000 ) ) ;
#27596=DIRECTION ( 'NONE',  ( -1.188678714063518227E-15, 1.000000000000000000, 3.263080277421930985E-16 ) ) ;
#27695=EDGE_LOOP ( 'NONE', ( #31117, #36674, #3749, #39113 ) ) ;
#27747=DIRECTION ( 'NONE',  ( 5.551115123125845564E-17, 0.000000000000000000, -1.000000000000000000 ) ) ;
#27756=PRODUCT_CONTEXT ( 'NONE', #11111, 'mechanical' ) ;
#27805=EDGE_CURVE ( 'NONE', #17210, #1749, #30382, .T. ) ;
#27819=AXIS2_PLACEMENT_3D ( 'NONE', #8920, #2961, #8315 ) ;
#27845=CARTESIAN_POINT ( 'NONE',  ( 2.048885995248197414E-16, 0.2900000000000004796, -5.122214988120493288E-16 ) ) ;
#27881=CARTESIAN_POINT ( 'NONE',  ( 2.072478234521481980E-16, 0.2900000000000004796, -0.04250000000000046102 ) ) ;
#27986=CLOSED_SHELL ( 'NONE', ( #7443, #8990, #37655, #10265, #37928, #11260, #666, #34530, #31417, #39798, #3962, #34181, #16948, #1992, #3843, #22069, #1166, #24143 ) ) ;
#28014=CARTESIAN_POINT ( 'NONE',  ( 5.463695987328526437E-16, -0.2899999999999993694, -7.171100983368691195E-16 ) ) ;
#28225=ORIENTED_EDGE ( 'NONE', *, *, #25869, .F. ) ;
#28234=EDGE_CURVE ( 'NONE', #14594, #23808, #16642, .T. ) ;
#28289=EDGE_CURVE ( 'NONE', #5485, #40210, #4782, .T. ) ;
#28300=EDGE_CURVE ( 'NONE', #1103, #23955, #38301, .T. ) ;
#28399=CARTESIAN_POINT ( 'NONE',  ( 5.330214113969031311E-16, -0.2899999999999993139, 0.07499999999999919231 ) ) ;
#28412=FACE_BOUND ( 'NONE', #11078, .T. ) ;
#28503=AXIS2_PLACEMENT_3D ( 'NONE', #11034, #35922, #27065 ) ;
#28609=TOROIDAL_SURFACE ( 'NONE', #23371, 0.04249999999999999611, 0.02499999999999995628 ) ;
#28767=EDGE_CURVE ( 'NONE', #40210, #2772, #33722, .T. ) ;
#28794=CARTESIAN_POINT ( 'NONE',  ( 2.048885995248197414E-16, 0.2981948553318907735, -1.707404996040164512E-16 ) ) ;
#28824=EDGE_CURVE ( 'NONE', #21571, #5485, #10811, .T. ) ;
#28847=EDGE_CURVE ( 'NONE', #11941, #1103, #35900, .T. ) ;
#29114=CARTESIAN_POINT ( 'NONE',  ( 4.816453576238493819E-16, 0.2949999999999991518, -0.06434668806854160206 ) ) ;
#29365=CIRCLE ( 'NONE', #33975, 0.04249999999999994754 ) ;
#29551=CARTESIAN_POINT ( 'NONE',  ( 5.543712964093851419E-16, -0.3059742766594579222, 0.06173076923076769446 ) ) ;
#29554=CARTESIAN_POINT ( 'NONE',  ( 2.048885995248197414E-16, 0.2900000000000004796, -5.122214988120493288E-16 ) ) ;
#29564=FACE_OUTER_BOUND ( 'NONE', #19726, .T. ) ;
#29598=ORIENTED_EDGE ( 'NONE', *, *, #28300, .F. ) ;
#29636=CARTESIAN_POINT ( 'NONE',  ( 1.893270629535517794E-16, 0.3059742766594581997, -0.06173076923076962347 ) ) ;
#29719=DIRECTION ( 'NONE',  ( 1.188678714063518227E-15, -1.000000000000000000, -3.263080277421930985E-16 ) ) ;
#29855=ORIENTED_EDGE ( 'NONE', *, *, #18217, .F. ) ;
#29892=CIRCLE ( 'NONE', #2294, 0.06173076923076910999 ) ;
#29904=EDGE_CURVE ( 'NONE', #14594, #14778, #23270, .T. ) ;
#29924=ORIENTED_EDGE ( 'NONE', *, *, #28289, .F. ) ;
#29967=DIRECTION ( 'NONE',  ( -1.188678714063518227E-15, 1.000000000000000000, 3.263080277421930985E-16 ) ) ;
#29990=DIRECTION ( 'NONE',  ( 5.551115123125788865E-17, -3.676620095425087714E-16, -1.000000000000000000 ) ) ;
#30078=AXIS2_PLACEMENT_3D ( 'NONE', #3375, #7825, #13055 ) ;
#30331=CARTESIAN_POINT ( 'NONE',  ( 2.099101141760805602E-16, 0.2900000000000004796, 0.07499999999999940048 ) ) ;
#30382=CIRCLE ( 'NONE', #35639, 0.06173076923076910999 ) ;
#30410=ORIENTED_EDGE ( 'NONE', *, *, #9712, .F. ) ;
#30767=EDGE_CURVE ( 'NONE', #21571, #7737, #29892, .T. ) ;
#30778=CARTESIAN_POINT ( 'NONE',  ( 1.171686751969803217E-18, -0.2899999999999993694, 0.01749999999999931818 ) ) ;
#30823=ORIENTED_EDGE ( 'NONE', *, *, #38890, .F. ) ;
#31091=DIRECTION ( 'NONE',  ( 1.188678714063530652E-15, -1.000000000000000000, 0.000000000000000000 ) ) ;
#31117=ORIENTED_EDGE ( 'NONE', *, *, #20570, .F. ) ;
#31159=CIRCLE ( 'NONE', #6183, 0.04249999999999994754 ) ;
#31236=ORIENTED_EDGE ( 'NONE', *, *, #20318, .F. ) ;
#31333=ORIENTED_EDGE ( 'NONE', *, *, #30767, .T. ) ;
#31385=DIRECTION ( 'NONE',  ( 1.188678714063518227E-15, -1.000000000000000000, -3.263080277421930985E-16 ) ) ;
#31417=ADVANCED_FACE ( 'NONE', ( #9569 ), #3000, .F. ) ;
#31421=CARTESIAN_POINT ( 'NONE',  ( 2.058600446713667573E-16, 0.2900000000000004796, -0.01750000000000052902 ) ) ;
#31644=DIRECTION ( 'NONE',  ( -1.188678714063518227E-15, 1.000000000000000000, 3.263080277421930985E-16 ) ) ;
#31741=AXIS2_PLACEMENT_3D ( 'NONE', #38876, #36004, #17285 ) ;
#31883=ORIENTED_EDGE ( 'NONE', *, *, #24733, .T. ) ;
#31966=EDGE_LOOP ( 'NONE', ( #39198, #21557, #4993, #39232 ) ) ;
#31973=EDGE_LOOP ( 'NONE', ( #32713, #20924, #945, #30410 ) ) ;
#32173=MANIFOLD_SOLID_BREP ( 'Mirror1', #27986 ) ;
#32436=VECTOR ( 'NONE', #9054, 39.37007874015748143 ) ;
#32708=DIRECTION ( 'NONE',  ( 5.551115123125799958E-17, -4.553079989440443628E-16, -1.000000000000000000 ) ) ;
#32713=ORIENTED_EDGE ( 'NONE', *, *, #19299, .F. ) ;
#32728=DIRECTION ( 'NONE',  ( 5.551115123125868984E-17, -5.531779426422974156E-16, -1.000000000000000000 ) ) ;
#33027=CARTESIAN_POINT ( 'NONE',  ( 2.048885995248197414E-16, 0.2900000000000004796, -5.122214988120493288E-16 ) ) ;
#33197=FACE_OUTER_BOUND ( 'NONE', #8136, .T. ) ;
#33252=ORIENTED_EDGE ( 'NONE', *, *, #13180, .F. ) ;
#33359=( NAMED_UNIT ( * ) PLANE_ANGLE_UNIT ( ) SI_UNIT ( $, .RADIAN. ) );
#33485=CARTESIAN_POINT ( 'NONE',  ( 1.997133008241153135E-16, 0.2981948553318907180, 0.06819284191469529577 ) ) ;
#33511=ORIENTED_EDGE ( 'NONE', *, *, #26995, .T. ) ;
#33575=AXIS2_PLACEMENT_3D ( 'NONE', #12045, #11643, #5442 ) ;
#33639=DIRECTION ( 'NONE',  ( 5.551115123125788865E-17, -3.676620095425087221E-16, -1.000000000000000000 ) ) ;
#33722=CIRCLE ( 'NONE', #27195, 0.005000000000000014849 ) ;
#33826=EDGE_CURVE ( 'NONE', #36494, #21571, #14715, .T. ) ;
#33878=EDGE_CURVE ( 'NONE', #27248, #14778, #26499, .T. ) ;
#33931=DIRECTION ( 'NONE',  ( -1.188678714063518424E-15, 1.000000000000000000, 0.000000000000000000 ) ) ;
#33936=DIRECTION ( 'NONE',  ( -5.551115123125767911E-17, 5.007578356027541926E-16, 1.000000000000000000 ) ) ;
#33975=AXIS2_PLACEMENT_3D ( 'NONE', #40190, #34023, #15097 ) ;
#33995=ORIENTED_EDGE ( 'NONE', *, *, #6117, .T. ) ;
#34023=DIRECTION ( 'NONE',  ( 1.188678714063518227E-15, -1.000000000000000000, -3.263080277421930985E-16 ) ) ;
#34167=( LENGTH_UNIT ( ) NAMED_UNIT ( * ) SI_UNIT ( $, .METRE. ) );
#34181=ADVANCED_FACE ( 'NONE', ( #15864, #28412 ), #7186, .T. ) ;
#34248=CARTESIAN_POINT ( 'NONE',  ( 5.463695987328526437E-16, -0.2899999999999993694, -7.171100983368691195E-16 ) ) ;
#34276=ORIENTED_EDGE ( 'NONE', *, *, #1612, .F. ) ;
#34356=DIRECTION ( 'NONE',  ( -1.000000000000000000, -1.188678714063518030E-15, -1.779758311459931231E-16 ) ) ;
#34530=ADVANCED_FACE ( 'NONE', ( #38817 ), #4272, .F. ) ;
#34596=CIRCLE ( 'NONE', #2392, 0.06173076923076910999 ) ;
#35074=UNCERTAINTY_MEASURE_WITH_UNIT (LENGTH_MEASURE( 1.000000000000000082E-05 ), #39522, 'distance_accuracy_value', 'NONE');
#35202=DIRECTION ( 'NONE',  ( 1.188678714063518030E-15, -1.000000000000000000, 3.676620095425087714E-16 ) ) ;
#35394=CARTESIAN_POINT ( 'NONE',  ( 0.07499999999999933109, 0.2900000000000004796, -5.122214988120493288E-16 ) ) ;
#35426=DIRECTION ( 'NONE',  ( 1.188678714063518227E-15, -1.000000000000000000, -3.263080277421930985E-16 ) ) ;
#35483=VECTOR ( 'NONE', #39703, 39.37007874015748854 ) ;
#35510=FACE_OUTER_BOUND ( 'NONE', #1543, .T. ) ;
#35569=ORIENTED_EDGE ( 'NONE', *, *, #19299, .T. ) ;
#35639=AXIS2_PLACEMENT_3D ( 'NONE', #12986, #21449, #37875 ) ;
#35671=CONICAL_SURFACE ( 'NONE', #36303, 0.07499999999999991396, 0.6931599075767558293 ) ;
#35692=CARTESIAN_POINT ( 'NONE',  ( 7.512581982576723358E-16, 0.3059742766594581997, -3.756290991288361679E-16 ) ) ;
#35832=AXIS2_PLACEMENT_3D ( 'NONE', #4320, #13975, #25956 ) ;
#35857=CIRCLE ( 'NONE', #8925, 0.01750000000000001554 ) ;
#35900=LINE ( 'NONE', #26443, #4174 ) ;
#35919=SHAPE_REPRESENTATION ( 'Pivot body rivet', ( #27819 ), #25262 ) ;
#35922=DIRECTION ( 'NONE',  ( 1.000000000000000000, 1.188678714063518030E-15, 5.551115123125745108E-17 ) ) ;
#35954=LINE ( 'NONE', #20328, #24092 ) ;
#36004=DIRECTION ( 'NONE',  ( 1.188678714063518227E-15, -1.000000000000000000, -3.263080277421930985E-16 ) ) ;
#36205=ORIENTED_EDGE ( 'NONE', *, *, #33826, .T. ) ;
#36244=CIRCLE ( 'NONE', #819, 0.06819284191469469902 ) ;
#36303=AXIS2_PLACEMENT_3D ( 'NONE', #2053, #17279, #32708 ) ;
#36356=ORIENTED_EDGE ( 'NONE', *, *, #25869, .T. ) ;
#36418=CARTESIAN_POINT ( 'NONE',  ( 2.090519358671640883E-16, 0.2900000000000004241, -0.07500000000000042744 ) ) ;
#36455=CARTESIAN_POINT ( 'NONE',  ( 5.463695987328526437E-16, -0.2899999999999993694, -7.171100983368691195E-16 ) ) ;
#36494=VERTEX_POINT ( 'NONE', #1506 ) ;
#36639=ORIENTED_EDGE ( 'NONE', *, *, #30767, .F. ) ;
#36651=FACE_OUTER_BOUND ( 'NONE', #20548, .T. ) ;
#36674=ORIENTED_EDGE ( 'NONE', *, *, #26115, .T. ) ;
#36687=CARTESIAN_POINT ( 'NONE',  ( 0.000000000000000000, 0.000000000000000000, 0.000000000000000000 ) ) ;
#36824=DIRECTION ( 'NONE',  ( -1.188678714063517635E-15, 1.000000000000000000, 0.000000000000000000 ) ) ;
#36836=DIRECTION ( 'NONE',  ( 5.551115123125718607E-17, 3.263080277421931478E-16, -1.000000000000000000 ) ) ;
#36873=AXIS2_PLACEMENT_3D ( 'NONE', #6442, #21692, #19015 ) ;
#36945=CARTESIAN_POINT ( 'NONE',  ( 2.084605582574230847E-16, 0.2900000000000004241, -0.06434668806854136613 ) ) ;
#37150=DIRECTION ( 'NONE',  ( 1.188678714063518227E-15, -1.000000000000000000, -3.263080277421930985E-16 ) ) ;
#37157=AXIS2_PLACEMENT_3D ( 'NONE', #28014, #25538, #12171 ) ;
#37195=CARTESIAN_POINT ( 'NONE',  ( 5.505329350751969413E-16, -0.2899999999999994249, -0.07500000000000062172 ) ) ;
#37306=ADVANCED_BREP_SHAPE_REPRESENTATION ( '', ( #32173, #27819 ), #25262 ) ;
#37451=CARTESIAN_POINT ( 'NONE',  ( 2.174026239640920213E-15, -0.2949999999999994293, 0.06434668806853986733 ) ) ;
#37486=ORIENTED_EDGE ( 'NONE', *, *, #16737, .T. ) ;
#37586=DIRECTION ( 'NONE',  ( 5.551115123125783935E-17, 0.000000000000000000, -1.000000000000000000 ) ) ;
#37655=ADVANCED_FACE ( 'NONE', ( #15657 ), #7569, .T. ) ;
#37707=AXIS2_PLACEMENT_3D ( 'NONE', #6626, #13033, #38112 ) ;
#37750=PLANE ( 'NONE',  #17622 ) ;
#37828=SHAPE_DEFINITION_REPRESENTATION ( #2158, #35919 ) ;
#37875=DIRECTION ( 'NONE',  ( 5.551115123125868984E-17, -5.531779426422974156E-16, -1.000000000000000000 ) ) ;
#37928=ADVANCED_FACE ( 'NONE', ( #1462 ), #19960, .T. ) ;
#37934=CARTESIAN_POINT ( 'NONE',  ( 5.598961119911192370E-16, -0.2981948553318921058, -0.06819284191469447698 ) ) ;
#38036=CARTESIAN_POINT ( 'NONE',  ( 2.185478394931410575E-15, -0.2949999999999994293, -9.902948977032954413E-16 ) ) ;
#38051=CARTESIAN_POINT ( 'NONE',  ( 5.388056259091479659E-16, -0.2899999999999993694, 0.04249999999999923284 ) ) ;
#38112=DIRECTION ( 'NONE',  ( -1.188678714063518819E-15, 1.000000000000000000, 0.000000000000000000 ) ) ;
#38194=CONICAL_SURFACE ( 'NONE', #33575, 0.07499999999999991396, 0.6931599075767558293 ) ;
#38289=AXIS2_PLACEMENT_3D ( 'NONE', #13533, #6940, #3456 ) ;
#38301=CIRCLE ( 'NONE', #8722, 0.04249999999999994754 ) ;
#38317=AXIS2_PLACEMENT_3D ( 'NONE', #35394, #35202, #19572 ) ;
#38358=EDGE_CURVE ( 'NONE', #36494, #8537, #35857, .T. ) ;
#38453=ORIENTED_EDGE ( 'NONE', *, *, #29904, .F. ) ;
#38555=AXIS2_PLACEMENT_3D ( 'NONE', #29554, #23422, #10848 ) ;
#38817=FACE_OUTER_BOUND ( 'NONE', #27267, .T. ) ;
#38876=CARTESIAN_POINT ( 'NONE',  ( 5.463695987328526437E-16, -0.2899999999999993694, -7.171100983368691195E-16 ) ) ;
#38890=EDGE_CURVE ( 'NONE', #7737, #21571, #34596, .T. ) ;
#38919=( LENGTH_UNIT ( ) NAMED_UNIT ( * ) SI_UNIT ( $, .METRE. ) );
#38966=AXIS2_PLACEMENT_3D ( 'NONE', #36687, #27239, #23742 ) ;
#38990=CARTESIAN_POINT ( 'NONE',  ( 2.048885995248197414E-16, 0.2900000000000004796, -5.122214988120493288E-16 ) ) ;
#39113=ORIENTED_EDGE ( 'NONE', *, *, #25547, .F. ) ;
#39198=ORIENTED_EDGE ( 'NONE', *, *, #38890, .T. ) ;
#39232=ORIENTED_EDGE ( 'NONE', *, *, #7717, .F. ) ;
#39353=ORIENTED_EDGE ( 'NONE', *, *, #27805, .F. ) ;
#39522=( CONVERSION_BASED_UNIT ( 'INCH', #26991 ) LENGTH_UNIT ( ) NAMED_UNIT ( #4161 ) );
#39531=CIRCLE ( 'NONE', #9980, 0.02499999999999993894 ) ;
#39688=FACE_OUTER_BOUND ( 'NONE', #31966, .T. ) ;
#39703=DIRECTION ( 'NONE',  ( 9.498382610854457704E-16, -0.7692307692307690514, -0.6389710663783134681 ) ) ;
#39798=ADVANCED_FACE ( 'NONE', ( #35510 ), #2421, .T. ) ;
#39826=DIRECTION ( 'NONE',  ( 5.551115123125759899E-17, -4.553079989440443628E-16, -1.000000000000000000 ) ) ;
#40075=EDGE_CURVE ( 'NONE', #2630, #2835, #23196, .T. ) ;
#40190=CARTESIAN_POINT ( 'NONE',  ( 2.048885995248197414E-16, 0.2900000000000004796, -5.122214988120493288E-16 ) ) ;
#40210=VERTEX_POINT ( 'NONE', #4047 ) ;
#40214=CARTESIAN_POINT ( 'NONE',  ( 0.000000000000000000, 0.000000000000000000, 0.000000000000000000 ) ) ;
#40667=COLOUR_RGB('Dark Blue',0.08,0.2,0.34);
#40668=FILL_AREA_STYLE_COLOUR('',#40667);
#40669=FILL_AREA_STYLE('',(#40668));
#40670=SURFACE_STYLE_FILL_AREA(#40669);
#40671=SURFACE_SIDE_STYLE('',(#40670));
#40672=SURFACE_STYLE_USAGE(.BOTH.,#40671);
#40673=PRESENTATION_STYLE_ASSIGNMENT((#40672));
#40712=STYLED_ITEM('',(#40673),#32173);
#40721=MECHANICAL_DESIGN_GEOMETRIC_PRESENTATION_REPRESENTATION('',(#40712),#11399);
ENDSEC;
END-ISO-10303-21;
